ISO-10303-21;
HEADER;
/* Generated by software containing ST-Developer
 * from STEP Tools, Inc. (www.steptools.com) 
 */

FILE_DESCRIPTION(
/* description */ (''),
/* implementation_level */ '2;1');

FILE_NAME(
/* name */ 'Screw_04.step',
/* time_stamp */ '2026-10-06T13:23:02-07:00',
/* author */ (''),
/* organization */ (''),
/* preprocessor_version */ 'ST-DEVELOPER v20.2',
/* originating_system */ 'Autodesk Translation Framework v15.15.0.0',
/* authorisation */ '');

FILE_SCHEMA (('AUTOMOTIVE_DESIGN { 1 0 10303 214 3 1 1 }'));
ENDSEC;

DATA;
#10=MECHANICAL_DESIGN_GEOMETRIC_PRESENTATION_REPRESENTATION('',(#74),#4994);
#54=SHAPE_REPRESENTATION_RELATIONSHIP('SRR','None',#5035,#64);
#64=ADVANCED_BREP_SHAPE_REPRESENTATION('',(#84),#4987);
#74=STYLED_ITEM('',(#5091),#84);
#84=MANIFOLD_SOLID_BREP('Body1',#2914);
#97=CYLINDRICAL_SURFACE('',#3123,1.9);
#98=CYLINDRICAL_SURFACE('',#3137,0.96675);
#129=FACE_BOUND('',#547,.T.);
#130=FACE_BOUND('',#564,.T.);
#211=PLANE('',#3122);
#212=PLANE('',#3125);
#213=PLANE('',#3126);
#214=PLANE('',#3127);
#215=PLANE('',#3128);
#216=PLANE('',#3129);
#217=PLANE('',#3130);
#218=PLANE('',#3131);
#219=PLANE('',#3132);
#220=PLANE('',#3133);
#221=PLANE('',#3134);
#222=PLANE('',#3135);
#223=PLANE('',#3136);
#224=PLANE('',#3139);
#225=PLANE('',#3140);
#302=TOROIDAL_SURFACE('',#3118,1.7,0.2);
#360=FACE_OUTER_BOUND('',#544,.T.);
#361=FACE_OUTER_BOUND('',#545,.T.);
#362=FACE_OUTER_BOUND('',#546,.T.);
#363=FACE_OUTER_BOUND('',#548,.T.);
#364=FACE_OUTER_BOUND('',#549,.T.);
#365=FACE_OUTER_BOUND('',#550,.T.);
#366=FACE_OUTER_BOUND('',#551,.T.);
#367=FACE_OUTER_BOUND('',#552,.T.);
#368=FACE_OUTER_BOUND('',#553,.T.);
#369=FACE_OUTER_BOUND('',#554,.T.);
#370=FACE_OUTER_BOUND('',#555,.T.);
#371=FACE_OUTER_BOUND('',#556,.T.);
#372=FACE_OUTER_BOUND('',#557,.T.);
#373=FACE_OUTER_BOUND('',#558,.T.);
#374=FACE_OUTER_BOUND('',#559,.T.);
#375=FACE_OUTER_BOUND('',#560,.T.);
#376=FACE_OUTER_BOUND('',#561,.T.);
#377=FACE_OUTER_BOUND('',#562,.T.);
#378=FACE_OUTER_BOUND('',#563,.T.);
#544=EDGE_LOOP('',(#2180,#2181,#2182,#2183));
#545=EDGE_LOOP('',(#2184,#2185,#2186,#2187));
#546=EDGE_LOOP('',(#2188));
#547=EDGE_LOOP('',(#2189,#2190,#2191,#2192,#2193,#2194));
#548=EDGE_LOOP('',(#2195,#2196,#2197,#2198));
#549=EDGE_LOOP('',(#2199,#2200,#2201));
#550=EDGE_LOOP('',(#2202,#2203,#2204));
#551=EDGE_LOOP('',(#2205,#2206,#2207));
#552=EDGE_LOOP('',(#2208,#2209,#2210));
#553=EDGE_LOOP('',(#2211,#2212,#2213));
#554=EDGE_LOOP('',(#2214,#2215,#2216));
#555=EDGE_LOOP('',(#2217,#2218,#2219,#2220));
#556=EDGE_LOOP('',(#2221,#2222,#2223,#2224));
#557=EDGE_LOOP('',(#2225,#2226,#2227,#2228));
#558=EDGE_LOOP('',(#2229,#2230,#2231,#2232));
#559=EDGE_LOOP('',(#2233,#2234,#2235,#2236));
#560=EDGE_LOOP('',(#2237,#2238,#2239,#2240));
#561=EDGE_LOOP('',(#2241,#2242,#2243,#2244));
#562=EDGE_LOOP('',(#2245));
#563=EDGE_LOOP('',(#2246));
#564=EDGE_LOOP('',(#2247));
#783=LINE('',#4390,#1076);
#784=LINE('',#4401,#1077);
#785=LINE('',#4403,#1078);
#786=LINE('',#4405,#1079);
#787=LINE('',#4407,#1080);
#788=LINE('',#4409,#1081);
#789=LINE('',#4410,#1082);
#790=LINE('',#4414,#1083);
#791=LINE('',#4418,#1084);
#792=LINE('',#4420,#1085);
#793=LINE('',#4421,#1086);
#794=LINE('',#4424,#1087);
#795=LINE('',#4425,#1088);
#796=LINE('',#4428,#1089);
#797=LINE('',#4429,#1090);
#798=LINE('',#4432,#1091);
#799=LINE('',#4433,#1092);
#800=LINE('',#4436,#1093);
#801=LINE('',#4437,#1094);
#802=LINE('',#4439,#1095);
#803=LINE('',#4441,#1096);
#804=LINE('',#4442,#1097);
#805=LINE('',#4444,#1098);
#806=LINE('',#4446,#1099);
#807=LINE('',#4448,#1100);
#808=LINE('',#4450,#1101);
#809=LINE('',#4454,#1102);
#1076=VECTOR('',#3563,0.887310000000001);
#1077=VECTOR('',#3576,10.);
#1078=VECTOR('',#3577,10.);
#1079=VECTOR('',#3578,10.);
#1080=VECTOR('',#3579,10.);
#1081=VECTOR('',#3580,10.);
#1082=VECTOR('',#3581,10.);
#1083=VECTOR('',#3586,1.9);
#1084=VECTOR('',#3589,9.99999999999999);
#1085=VECTOR('',#3590,10.);
#1086=VECTOR('',#3591,10.);
#1087=VECTOR('',#3594,10.);
#1088=VECTOR('',#3595,10.);
#1089=VECTOR('',#3598,10.);
#1090=VECTOR('',#3599,9.99999999999999);
#1091=VECTOR('',#3602,10.);
#1092=VECTOR('',#3603,10.);
#1093=VECTOR('',#3606,10.);
#1094=VECTOR('',#3607,10.);
#1095=VECTOR('',#3610,10.);
#1096=VECTOR('',#3613,10.);
#1097=VECTOR('',#3614,10.);
#1098=VECTOR('',#3617,10.);
#1099=VECTOR('',#3620,10.);
#1100=VECTOR('',#3623,10.);
#1101=VECTOR('',#3626,10.);
#1102=VECTOR('',#3631,0.96675);
#1309=CIRCLE('',#3116,0.96675);
#1310=CIRCLE('',#3117,0.754619999999998);
#1311=CIRCLE('',#3119,1.9);
#1312=CIRCLE('',#3120,0.2);
#1313=CIRCLE('',#3121,1.7);
#1314=CIRCLE('',#3124,1.9);
#1315=CIRCLE('',#3138,0.96675);
#1426=VERTEX_POINT('',#4387);
#1427=VERTEX_POINT('',#4389);
#1428=VERTEX_POINT('',#4393);
#1429=VERTEX_POINT('',#4395);
#1430=VERTEX_POINT('',#4399);
#1431=VERTEX_POINT('',#4400);
#1432=VERTEX_POINT('',#4402);
#1433=VERTEX_POINT('',#4404);
#1434=VERTEX_POINT('',#4406);
#1435=VERTEX_POINT('',#4408);
#1436=VERTEX_POINT('',#4412);
#1437=VERTEX_POINT('',#4416);
#1438=VERTEX_POINT('',#4417);
#1439=VERTEX_POINT('',#4419);
#1440=VERTEX_POINT('',#4423);
#1441=VERTEX_POINT('',#4427);
#1442=VERTEX_POINT('',#4431);
#1443=VERTEX_POINT('',#4435);
#1444=VERTEX_POINT('',#4453);
#1704=EDGE_CURVE('',#1426,#1426,#1309,.T.);
#1705=EDGE_CURVE('',#1426,#1427,#783,.T.);
#1706=EDGE_CURVE('',#1427,#1427,#1310,.T.);
#1707=EDGE_CURVE('',#1428,#1428,#1311,.T.);
#1708=EDGE_CURVE('',#1428,#1429,#1312,.T.);
#1709=EDGE_CURVE('',#1429,#1429,#1313,.T.);
#1710=EDGE_CURVE('',#1430,#1431,#784,.T.);
#1711=EDGE_CURVE('',#1431,#1432,#785,.T.);
#1712=EDGE_CURVE('',#1432,#1433,#786,.T.);
#1713=EDGE_CURVE('',#1433,#1434,#787,.T.);
#1714=EDGE_CURVE('',#1434,#1435,#788,.T.);
#1715=EDGE_CURVE('',#1435,#1430,#789,.T.);
#1716=EDGE_CURVE('',#1436,#1436,#1314,.T.);
#1717=EDGE_CURVE('',#1436,#1428,#790,.T.);
#1718=EDGE_CURVE('',#1437,#1438,#791,.T.);
#1719=EDGE_CURVE('',#1439,#1437,#792,.T.);
#1720=EDGE_CURVE('',#1439,#1438,#793,.T.);
#1721=EDGE_CURVE('',#1440,#1439,#794,.T.);
#1722=EDGE_CURVE('',#1440,#1438,#795,.T.);
#1723=EDGE_CURVE('',#1441,#1440,#796,.T.);
#1724=EDGE_CURVE('',#1441,#1438,#797,.T.);
#1725=EDGE_CURVE('',#1442,#1441,#798,.T.);
#1726=EDGE_CURVE('',#1442,#1438,#799,.T.);
#1727=EDGE_CURVE('',#1443,#1442,#800,.T.);
#1728=EDGE_CURVE('',#1443,#1438,#801,.T.);
#1729=EDGE_CURVE('',#1437,#1443,#802,.T.);
#1730=EDGE_CURVE('',#1430,#1439,#803,.T.);
#1731=EDGE_CURVE('',#1431,#1437,#804,.T.);
#1732=EDGE_CURVE('',#1435,#1440,#805,.T.);
#1733=EDGE_CURVE('',#1434,#1441,#806,.T.);
#1734=EDGE_CURVE('',#1433,#1442,#807,.T.);
#1735=EDGE_CURVE('',#1432,#1443,#808,.T.);
#1736=EDGE_CURVE('',#1426,#1444,#809,.T.);
#1737=EDGE_CURVE('',#1444,#1444,#1315,.F.);
#2180=ORIENTED_EDGE('',*,*,#1704,.F.);
#2181=ORIENTED_EDGE('',*,*,#1705,.T.);
#2182=ORIENTED_EDGE('',*,*,#1706,.F.);
#2183=ORIENTED_EDGE('',*,*,#1705,.F.);
#2184=ORIENTED_EDGE('',*,*,#1707,.T.);
#2185=ORIENTED_EDGE('',*,*,#1708,.T.);
#2186=ORIENTED_EDGE('',*,*,#1709,.T.);
#2187=ORIENTED_EDGE('',*,*,#1708,.F.);
#2188=ORIENTED_EDGE('',*,*,#1709,.F.);
#2189=ORIENTED_EDGE('',*,*,#1710,.T.);
#2190=ORIENTED_EDGE('',*,*,#1711,.T.);
#2191=ORIENTED_EDGE('',*,*,#1712,.T.);
#2192=ORIENTED_EDGE('',*,*,#1713,.T.);
#2193=ORIENTED_EDGE('',*,*,#1714,.T.);
#2194=ORIENTED_EDGE('',*,*,#1715,.T.);
#2195=ORIENTED_EDGE('',*,*,#1716,.F.);
#2196=ORIENTED_EDGE('',*,*,#1717,.T.);
#2197=ORIENTED_EDGE('',*,*,#1707,.F.);
#2198=ORIENTED_EDGE('',*,*,#1717,.F.);
#2199=ORIENTED_EDGE('',*,*,#1718,.F.);
#2200=ORIENTED_EDGE('',*,*,#1719,.F.);
#2201=ORIENTED_EDGE('',*,*,#1720,.T.);
#2202=ORIENTED_EDGE('',*,*,#1720,.F.);
#2203=ORIENTED_EDGE('',*,*,#1721,.F.);
#2204=ORIENTED_EDGE('',*,*,#1722,.T.);
#2205=ORIENTED_EDGE('',*,*,#1722,.F.);
#2206=ORIENTED_EDGE('',*,*,#1723,.F.);
#2207=ORIENTED_EDGE('',*,*,#1724,.T.);
#2208=ORIENTED_EDGE('',*,*,#1724,.F.);
#2209=ORIENTED_EDGE('',*,*,#1725,.F.);
#2210=ORIENTED_EDGE('',*,*,#1726,.T.);
#2211=ORIENTED_EDGE('',*,*,#1726,.F.);
#2212=ORIENTED_EDGE('',*,*,#1727,.F.);
#2213=ORIENTED_EDGE('',*,*,#1728,.T.);
#2214=ORIENTED_EDGE('',*,*,#1728,.F.);
#2215=ORIENTED_EDGE('',*,*,#1729,.F.);
#2216=ORIENTED_EDGE('',*,*,#1718,.T.);
#2217=ORIENTED_EDGE('',*,*,#1710,.F.);
#2218=ORIENTED_EDGE('',*,*,#1730,.T.);
#2219=ORIENTED_EDGE('',*,*,#1719,.T.);
#2220=ORIENTED_EDGE('',*,*,#1731,.F.);
#2221=ORIENTED_EDGE('',*,*,#1715,.F.);
#2222=ORIENTED_EDGE('',*,*,#1732,.T.);
#2223=ORIENTED_EDGE('',*,*,#1721,.T.);
#2224=ORIENTED_EDGE('',*,*,#1730,.F.);
#2225=ORIENTED_EDGE('',*,*,#1714,.F.);
#2226=ORIENTED_EDGE('',*,*,#1733,.T.);
#2227=ORIENTED_EDGE('',*,*,#1723,.T.);
#2228=ORIENTED_EDGE('',*,*,#1732,.F.);
#2229=ORIENTED_EDGE('',*,*,#1713,.F.);
#2230=ORIENTED_EDGE('',*,*,#1734,.T.);
#2231=ORIENTED_EDGE('',*,*,#1725,.T.);
#2232=ORIENTED_EDGE('',*,*,#1733,.F.);
#2233=ORIENTED_EDGE('',*,*,#1712,.F.);
#2234=ORIENTED_EDGE('',*,*,#1735,.T.);
#2235=ORIENTED_EDGE('',*,*,#1727,.T.);
#2236=ORIENTED_EDGE('',*,*,#1734,.F.);
#2237=ORIENTED_EDGE('',*,*,#1711,.F.);
#2238=ORIENTED_EDGE('',*,*,#1731,.T.);
#2239=ORIENTED_EDGE('',*,*,#1729,.T.);
#2240=ORIENTED_EDGE('',*,*,#1735,.F.);
#2241=ORIENTED_EDGE('',*,*,#1704,.T.);
#2242=ORIENTED_EDGE('',*,*,#1736,.T.);
#2243=ORIENTED_EDGE('',*,*,#1737,.T.);
#2244=ORIENTED_EDGE('',*,*,#1736,.F.);
#2245=ORIENTED_EDGE('',*,*,#1706,.T.);
#2246=ORIENTED_EDGE('',*,*,#1716,.T.);
#2247=ORIENTED_EDGE('',*,*,#1737,.F.);
#2727=CONICAL_SURFACE('',#3115,0.887310000000001,0.824535502685815);
#2790=ADVANCED_FACE('',(#360),#2727,.T.);
#2791=ADVANCED_FACE('',(#361),#302,.T.);
#2792=ADVANCED_FACE('',(#362,#129),#211,.T.);
#2793=ADVANCED_FACE('',(#363),#97,.T.);
#2794=ADVANCED_FACE('',(#364),#212,.F.);
#2795=ADVANCED_FACE('',(#365),#213,.F.);
#2796=ADVANCED_FACE('',(#366),#214,.F.);
#2797=ADVANCED_FACE('',(#367),#215,.F.);
#2798=ADVANCED_FACE('',(#368),#216,.F.);
#2799=ADVANCED_FACE('',(#369),#217,.F.);
#2800=ADVANCED_FACE('',(#370),#218,.F.);
#2801=ADVANCED_FACE('',(#371),#219,.F.);
#2802=ADVANCED_FACE('',(#372),#220,.F.);
#2803=ADVANCED_FACE('',(#373),#221,.F.);
#2804=ADVANCED_FACE('',(#374),#222,.F.);
#2805=ADVANCED_FACE('',(#375),#223,.F.);
#2806=ADVANCED_FACE('',(#376),#98,.T.);
#2807=ADVANCED_FACE('',(#377),#224,.T.);
#2808=ADVANCED_FACE('',(#378,#130),#225,.T.);
#2914=CLOSED_SHELL('',(#2790,#2791,#2792,#2793,#2794,#2795,#2796,#2797,
#2798,#2799,#2800,#2801,#2802,#2803,#2804,#2805,#2806,#2807,#2808));
#3114=AXIS2_PLACEMENT_3D('',#4385,#3557,#3558);
#3115=AXIS2_PLACEMENT_3D('',#4386,#3559,#3560);
#3116=AXIS2_PLACEMENT_3D('',#4388,#3561,#3562);
#3117=AXIS2_PLACEMENT_3D('',#4391,#3564,#3565);
#3118=AXIS2_PLACEMENT_3D('',#4392,#3566,#3567);
#3119=AXIS2_PLACEMENT_3D('',#4394,#3568,#3569);
#3120=AXIS2_PLACEMENT_3D('',#4396,#3570,#3571);
#3121=AXIS2_PLACEMENT_3D('',#4397,#3572,#3573);
#3122=AXIS2_PLACEMENT_3D('',#4398,#3574,#3575);
#3123=AXIS2_PLACEMENT_3D('',#4411,#3582,#3583);
#3124=AXIS2_PLACEMENT_3D('',#4413,#3584,#3585);
#3125=AXIS2_PLACEMENT_3D('',#4415,#3587,#3588);
#3126=AXIS2_PLACEMENT_3D('',#4422,#3592,#3593);
#3127=AXIS2_PLACEMENT_3D('',#4426,#3596,#3597);
#3128=AXIS2_PLACEMENT_3D('',#4430,#3600,#3601);
#3129=AXIS2_PLACEMENT_3D('',#4434,#3604,#3605);
#3130=AXIS2_PLACEMENT_3D('',#4438,#3608,#3609);
#3131=AXIS2_PLACEMENT_3D('',#4440,#3611,#3612);
#3132=AXIS2_PLACEMENT_3D('',#4443,#3615,#3616);
#3133=AXIS2_PLACEMENT_3D('',#4445,#3618,#3619);
#3134=AXIS2_PLACEMENT_3D('',#4447,#3621,#3622);
#3135=AXIS2_PLACEMENT_3D('',#4449,#3624,#3625);
#3136=AXIS2_PLACEMENT_3D('',#4451,#3627,#3628);
#3137=AXIS2_PLACEMENT_3D('',#4452,#3629,#3630);
#3138=AXIS2_PLACEMENT_3D('',#4455,#3632,#3633);
#3139=AXIS2_PLACEMENT_3D('',#4456,#3634,#3635);
#3140=AXIS2_PLACEMENT_3D('',#4457,#3636,#3637);
#3557=DIRECTION('axis',(0.,0.,1.));
#3558=DIRECTION('refdir',(1.,0.,0.));
#3559=DIRECTION('center_axis',(0.,0.,1.));
#3560=DIRECTION('ref_axis',(-1.,0.,0.));
#3561=DIRECTION('center_axis',(-1.06387651071382E-15,0.,1.));
#3562=DIRECTION('ref_axis',(-1.,0.,-1.06387651071382E-15));
#3563=DIRECTION('',(-0.73423251512767,-8.99175499481012E-17,-0.678898087881602));
#3564=DIRECTION('center_axis',(1.06387651071382E-15,0.,-1.));
#3565=DIRECTION('ref_axis',(-1.,0.,-1.06387651071382E-15));
#3566=DIRECTION('center_axis',(1.06387651071382E-15,0.,-1.));
#3567=DIRECTION('ref_axis',(-1.,0.,-1.05179023385541E-15));
#3568=DIRECTION('center_axis',(-1.06387651071382E-15,0.,1.));
#3569=DIRECTION('ref_axis',(1.,0.,1.06387651071382E-15));
#3570=DIRECTION('center_axis',(-1.22464679914735E-16,-1.,-1.30287296353373E-31));
#3571=DIRECTION('ref_axis',(1.,-1.22464679914735E-16,1.02257383847054E-15));
#3572=DIRECTION('center_axis',(1.06387651071382E-15,0.,-1.));
#3573=DIRECTION('ref_axis',(1.,0.,1.06387651071382E-15));
#3574=DIRECTION('center_axis',(-1.06387651071382E-15,0.,1.));
#3575=DIRECTION('ref_axis',(1.,0.,1.06387651071382E-15));
#3576=DIRECTION('',(-0.866025403784439,-0.5,-9.21344084767719E-16));
#3577=DIRECTION('',(-0.866025403784439,0.5,-9.21344084767719E-16));
#3578=DIRECTION('',(6.40987562127854E-16,1.,6.81931611007542E-31));
#3579=DIRECTION('',(0.866025403784439,0.5,9.21344084767719E-16));
#3580=DIRECTION('',(0.866025403784439,-0.5,9.21344084767719E-16));
#3581=DIRECTION('',(-1.60246890531964E-16,-1.,-1.70482902751885E-31));
#3582=DIRECTION('center_axis',(1.06387651071382E-15,0.,-1.));
#3583=DIRECTION('ref_axis',(-1.,0.,-1.06387651071382E-15));
#3584=DIRECTION('center_axis',(1.06387651071382E-15,0.,-1.));
#3585=DIRECTION('ref_axis',(1.,0.,1.06387651071382E-15));
#3586=DIRECTION('',(-1.06387651071382E-15,0.,1.));
#3587=DIRECTION('center_axis',(0.0435778713738291,-0.0754790873051733,-0.996194698091746));
#3588=DIRECTION('ref_axis',(-0.866025403784439,-0.5,-3.35810244624808E-17));
#3589=DIRECTION('',(0.,0.997141949694316,-0.0755508581011305));
#3590=DIRECTION('',(-0.866025403784439,-0.5,0.));
#3591=DIRECTION('',(-0.863550259614423,0.498570974847158,-0.0755508581011305));
#3592=DIRECTION('center_axis',(0.0871557427476581,-1.3966436767316E-17,
-0.996194698091746));
#3593=DIRECTION('ref_axis',(-1.60246890531964E-16,-1.,1.77292017095641E-32));
#3594=DIRECTION('',(-1.60246890531964E-16,-1.,0.));
#3595=DIRECTION('',(-0.863550259614423,-0.498570974847158,-0.0755508581011305));
#3596=DIRECTION('center_axis',(0.0435778713738291,0.0754790873051733,-0.996194698091746));
#3597=DIRECTION('ref_axis',(0.866025403784439,-0.5,3.35810244624808E-17));
#3598=DIRECTION('',(0.866025403784439,-0.5,0.));
#3599=DIRECTION('',(-1.59381164582915E-16,-0.997141949694316,-0.0755508581011305));
#3600=DIRECTION('center_axis',(-0.0435778713738291,0.0754790873051733,-0.996194698091746));
#3601=DIRECTION('ref_axis',(0.866025403784439,0.5,-3.35810244624808E-17));
#3602=DIRECTION('',(0.866025403784439,0.5,0.));
#3603=DIRECTION('',(0.863550259614423,-0.498570974847159,-0.0755508581011305));
#3604=DIRECTION('center_axis',(-0.0871557427476581,5.58657470692638E-17,
-0.996194698091746));
#3605=DIRECTION('ref_axis',(6.40987562127854E-16,1.,4.7015367027096E-32));
#3606=DIRECTION('',(6.40987562127854E-16,1.,0.));
#3607=DIRECTION('',(0.863550259614423,0.498570974847158,-0.0755508581011305));
#3608=DIRECTION('center_axis',(-0.0435778713738291,-0.0754790873051733,
-0.996194698091746));
#3609=DIRECTION('ref_axis',(-0.866025403784439,0.5,3.35810244624808E-17));
#3610=DIRECTION('',(-0.866025403784439,0.5,0.));
#3611=DIRECTION('center_axis',(0.5,-0.866025403784439,0.));
#3612=DIRECTION('ref_axis',(-0.866025403784439,-0.5,0.));
#3613=DIRECTION('',(0.,0.,-1.));
#3614=DIRECTION('',(0.,0.,-1.));
#3615=DIRECTION('center_axis',(1.,-1.60246890531964E-16,0.));
#3616=DIRECTION('ref_axis',(-1.60246890531964E-16,-1.,0.));
#3617=DIRECTION('',(0.,0.,-1.));
#3618=DIRECTION('center_axis',(0.5,0.866025403784439,0.));
#3619=DIRECTION('ref_axis',(0.866025403784439,-0.5,0.));
#3620=DIRECTION('',(0.,0.,-1.));
#3621=DIRECTION('center_axis',(-0.5,0.866025403784439,0.));
#3622=DIRECTION('ref_axis',(0.866025403784439,0.5,0.));
#3623=DIRECTION('',(0.,0.,-1.));
#3624=DIRECTION('center_axis',(-1.,6.40987562127854E-16,0.));
#3625=DIRECTION('ref_axis',(6.40987562127854E-16,1.,0.));
#3626=DIRECTION('',(0.,0.,-1.));
#3627=DIRECTION('center_axis',(-0.5,-0.866025403784439,0.));
#3628=DIRECTION('ref_axis',(-0.866025403784439,0.5,0.));
#3629=DIRECTION('center_axis',(1.06387651071382E-15,0.,-1.));
#3630=DIRECTION('ref_axis',(-1.,0.,-1.06387651071382E-15));
#3631=DIRECTION('',(-1.06387651071382E-15,0.,1.));
#3632=DIRECTION('center_axis',(-1.06387651071382E-15,0.,1.));
#3633=DIRECTION('ref_axis',(-1.,0.,-1.06387651071382E-15));
#3634=DIRECTION('center_axis',(1.06387651071382E-15,0.,-1.));
#3635=DIRECTION('ref_axis',(-1.,0.,-1.06387651071382E-15));
#3636=DIRECTION('center_axis',(1.06387651071382E-15,0.,-1.));
#3637=DIRECTION('ref_axis',(-1.,0.,-1.06387651071382E-15));
#4385=CARTESIAN_POINT('',(0.,0.,0.));
#4386=CARTESIAN_POINT('Origin',(0.,0.,-4.87731));
#4387=CARTESIAN_POINT('',(0.966750000000005,1.1839272930757E-16,-4.80385688672847));
#4388=CARTESIAN_POINT('Origin',(5.11071050262126E-15,0.,-4.80385688672847));
#4389=CARTESIAN_POINT('',(0.754619999999998,-9.24142967572573E-17,-5.));
#4390=CARTESIAN_POINT('',(0.887310000000001,1.08664135135144E-16,-4.87731));
#4391=CARTESIAN_POINT('Origin',(0.,0.,-5.));
#4392=CARTESIAN_POINT('Origin',(-1.91497771928438E-15,0.,1.79999999999952));
#4393=CARTESIAN_POINT('',(1.89999999999999,-2.32682891837997E-16,1.79999999999953));
#4394=CARTESIAN_POINT('Origin',(-1.91497771928438E-15,0.,1.79999999999952));
#4395=CARTESIAN_POINT('',(1.69999999999999,-2.0818995585505E-16,1.99999999999953));
#4396=CARTESIAN_POINT('Origin',(1.7,-2.0818995585505E-16,1.79999999999952));
#4397=CARTESIAN_POINT('Origin',(-2.12775302142714E-15,0.,1.99999999999952));
#4398=CARTESIAN_POINT('Origin',(-1.9,0.,1.99999999999952));
#4399=CARTESIAN_POINT('',(0.75,-0.433012701892219,2.));
#4400=CARTESIAN_POINT('',(1.38777878078145E-16,-0.866025403784439,2.));
#4401=CARTESIAN_POINT('',(-0.149999999999999,-0.952627944162883,1.99999999999952));
#4402=CARTESIAN_POINT('',(-0.750000000000001,-0.433012701892219,2.));
#4403=CARTESIAN_POINT('',(-0.899999999999999,-0.346410161513776,1.99999999999952));
#4404=CARTESIAN_POINT('',(-0.75,0.43301270189222,2.));
#4405=CARTESIAN_POINT('',(-0.75,-0.21650635094611,1.99999999999952));
#4406=CARTESIAN_POINT('',(1.73472347597681E-17,0.866025403784439,2.));
#4407=CARTESIAN_POINT('',(-1.275,0.129903810567666,1.99999999999952));
#4408=CARTESIAN_POINT('',(0.75,0.433012701892219,2.));
#4409=CARTESIAN_POINT('',(-0.524999999999999,1.16913429510899,1.99999999999952));
#4410=CARTESIAN_POINT('',(0.75,0.216506350946109,1.99999999999952));
#4411=CARTESIAN_POINT('Origin',(-1.06387651071333E-15,0.,0.999999999999538));
#4412=CARTESIAN_POINT('',(1.9,-2.32682891837997E-16,-4.47419878923938E-13));
#4413=CARTESIAN_POINT('Origin',(4.74691816123085E-28,0.,-4.48558184615945E-13));
#4414=CARTESIAN_POINT('',(1.9,-2.32682891837997E-16,0.99999999999954));
#4415=CARTESIAN_POINT('Origin',(1.38777878078145E-16,-0.866025403784439,
1.));
#4416=CARTESIAN_POINT('',(1.38777878078145E-16,-0.866025403784439,1.));
#4417=CARTESIAN_POINT('',(0.,2.77555756156289E-16,0.934383502355557));
#4418=CARTESIAN_POINT('',(0.,-0.650754856401699,0.983689509218169));
#4419=CARTESIAN_POINT('',(0.75,-0.433012701892219,1.));
#4420=CARTESIAN_POINT('',(8.5846548499269E-17,-0.866025403784439,1.));
#4421=CARTESIAN_POINT('',(0.563570237279966,-0.325377428200849,0.983689509218169));
#4422=CARTESIAN_POINT('Origin',(0.75,-0.433012701892219,1.));
#4423=CARTESIAN_POINT('',(0.75,0.433012701892219,1.));
#4424=CARTESIAN_POINT('',(0.75,-0.433012701892219,1.));
#4425=CARTESIAN_POINT('',(0.563570237279966,0.32537742820085,0.983689509218169));
#4426=CARTESIAN_POINT('Origin',(0.75,0.433012701892219,1.));
#4427=CARTESIAN_POINT('',(0.,0.866025403784439,1.));
#4428=CARTESIAN_POINT('',(0.75,0.433012701892219,1.));
#4429=CARTESIAN_POINT('',(0.,0.650754856401699,0.983689509218169));
#4430=CARTESIAN_POINT('Origin',(0.,0.866025403784439,1.));
#4431=CARTESIAN_POINT('',(-0.75,0.43301270189222,1.));
#4432=CARTESIAN_POINT('',(1.73472347597681E-17,0.866025403784439,1.));
#4433=CARTESIAN_POINT('',(-0.563570237279966,0.325377428200849,0.983689509218169));
#4434=CARTESIAN_POINT('Origin',(-0.75,0.43301270189222,1.));
#4435=CARTESIAN_POINT('',(-0.750000000000001,-0.433012701892219,1.));
#4436=CARTESIAN_POINT('',(-0.75,0.43301270189222,1.));
#4437=CARTESIAN_POINT('',(-0.563570237279966,-0.325377428200849,0.983689509218169));
#4438=CARTESIAN_POINT('Origin',(-0.750000000000001,-0.433012701892219,1.));
#4439=CARTESIAN_POINT('',(-0.750000000000001,-0.433012701892219,1.));
#4440=CARTESIAN_POINT('Origin',(0.75,-0.433012701892219,2.));
#4441=CARTESIAN_POINT('',(0.75,-0.433012701892219,2.));
#4442=CARTESIAN_POINT('',(1.38777878078145E-16,-0.866025403784439,2.));
#4443=CARTESIAN_POINT('Origin',(0.75,0.433012701892219,2.));
#4444=CARTESIAN_POINT('',(0.75,0.433012701892219,2.));
#4445=CARTESIAN_POINT('Origin',(0.,0.866025403784439,2.));
#4446=CARTESIAN_POINT('',(1.73472347597681E-17,0.866025403784439,2.));
#4447=CARTESIAN_POINT('Origin',(-0.75,0.43301270189222,2.));
#4448=CARTESIAN_POINT('',(-0.75,0.43301270189222,2.));
#4449=CARTESIAN_POINT('Origin',(-0.750000000000001,-0.433012701892219,2.));
#4450=CARTESIAN_POINT('',(-0.750000000000001,-0.433012701892219,2.));
#4451=CARTESIAN_POINT('Origin',(1.38777878078145E-16,-0.866025403784439,
2.));
#4452=CARTESIAN_POINT('Origin',(2.65969127678468E-15,0.,-2.50000000000012));
#4453=CARTESIAN_POINT('',(0.96675,1.1839272930757E-16,-2.35150733091162E-13));
#4454=CARTESIAN_POINT('',(0.966750000000003,-1.1839272930757E-16,-2.50000000000012));
#4455=CARTESIAN_POINT('Origin',(2.48491185144619E-28,0.,-2.35922392732846E-13));
#4456=CARTESIAN_POINT('Origin',(5.27355936696949E-15,0.,-5.));
#4457=CARTESIAN_POINT('Origin',(-0.999999999999996,0.,-2.37147131571737E-13));
#4975=UNCERTAINTY_MEASURE_WITH_UNIT(LENGTH_MEASURE(0.01),#4995,
'DISTANCE_ACCURACY_VALUE',
'Maximum model space distance between geometric entities at asserted c
onnectivities');
#4982=UNCERTAINTY_MEASURE_WITH_UNIT(LENGTH_MEASURE(0.01),#4995,
'DISTANCE_ACCURACY_VALUE',
'Maximum model space distance between geometric entities at asserted c
onnectivities');
#4987=(
GEOMETRIC_REPRESENTATION_CONTEXT(3)
GLOBAL_UNCERTAINTY_ASSIGNED_CONTEXT((#4975))
GLOBAL_UNIT_ASSIGNED_CONTEXT((#4995,#4997,#4998))
REPRESENTATION_CONTEXT('','3D')
);
#4994=(
GEOMETRIC_REPRESENTATION_CONTEXT(3)
GLOBAL_UNCERTAINTY_ASSIGNED_CONTEXT((#4982))
GLOBAL_UNIT_ASSIGNED_CONTEXT((#4995,#4997,#4998))
REPRESENTATION_CONTEXT('','3D')
);
#4995=(
LENGTH_UNIT()
NAMED_UNIT(*)
SI_UNIT(.MILLI.,.METRE.)
);
#4997=(
NAMED_UNIT(*)
PLANE_ANGLE_UNIT()
SI_UNIT($,.RADIAN.)
);
#4998=(
NAMED_UNIT(*)
SI_UNIT($,.STERADIAN.)
SOLID_ANGLE_UNIT()
);
#5003=SHAPE_DEFINITION_REPRESENTATION(#5014,#5035);
#5014=PRODUCT_DEFINITION_SHAPE('',$,#5047);
#5035=SHAPE_REPRESENTATION('',(#3114),#4987);
#5042=PRODUCT_DEFINITION_CONTEXT('part definition',#5077,'design');
#5047=PRODUCT_DEFINITION(
'BSHCS ASME B18.3.1M - M2x0.4 x 5 Steel Grade 2 Plain_3','Screw_04',#5058,
#5042);
#5058=PRODUCT_DEFINITION_FORMATION('',$,#5083);
#5077=APPLICATION_CONTEXT(
'Core Data for Automotive Mechanical Design Process');
#5078=PRODUCT_CONTEXT('part definition',#5077,'mechanical');
#5083=PRODUCT('BSHCS ASME B18.3.1M - M2x0.4 x 5 Steel Grade 2 Plain_3',
'Screw_04',
'Broached Hexagon Socket Head Cap Screw ASME B18.3.1M - M2x0.4 x 5',(#5078));
#5091=PRESENTATION_STYLE_ASSIGNMENT((#5096));
#5096=SURFACE_STYLE_USAGE(.BOTH.,#5101);
#5101=SURFACE_SIDE_STYLE('',(#5106));
#5106=SURFACE_STYLE_FILL_AREA(#5111);
#5111=FILL_AREA_STYLE('Opaque(160,160,160)',(#5116));
#5116=FILL_AREA_STYLE_COLOUR('Opaque(160,160,160)',#5121);
#5121=COLOUR_RGB('Opaque(160,160,160)', 0.09019608, 0.27058824, 0.51372549);
ENDSEC;
END-ISO-10303-21;
